ISO-10303-21;
HEADER;
FILE_DESCRIPTION (('STEP AP214'),
    '1' );
FILE_NAME ('Plunger Rod.step',
    '2026-10-06T09:00:30',
    ( '' ),
    ( '' ),
    'SwSTEP 2.0',
    'SolidWorks 2020',
    '' );
FILE_SCHEMA (( 'AUTOMOTIVE_DESIGN' ));
ENDSEC;

DATA;
#121=MANIFOLD_SOLID_BREP ( 'Stock-MAS-156-1', #21607 ) ;
#135=ORIENTED_EDGE ( 'NONE', *, *, #1841, .T. ) ;
#215=CIRCLE ( 'NONE', #4748, 1.500000000000000222 ) ;
#229=DIRECTION ( 'NONE',  ( -0.1090476345695678556, -0.6986477033489640887, -0.7071067811865474617 ) ) ;
#244=DIRECTION ( 'NONE',  ( 0.9880370573969197157, -0.1542166437529880196, 2.958228394580000263E-31 ) ) ;
#248=CARTESIAN_POINT ( 'NONE',  ( 2.914123423709013228, 2.127246859543532764, -88.52261276242110455 ) ) ;
#336=( NAMED_UNIT ( * ) PLANE_ANGLE_UNIT ( ) SI_UNIT ( $, .RADIAN. ) );
#397=AXIS2_PLACEMENT_3D ( 'NONE', #28615, #21537, #4694 ) ;
#403=CARTESIAN_POINT ( 'NONE',  ( 0.5564057544863512117, 3.564787113782302619, -88.52261276243972077 ) ) ;
#561=CARTESIAN_POINT ( 'NONE',  ( 3.371793442757397230, -0.3929169320064240245, -94.29636648343951322 ) ) ;
#576=LINE ( 'NONE', #10157, #14540 ) ;
#700=FACE_OUTER_BOUND ( 'NONE', #10031, .T. ) ;
#790=VERTEX_POINT ( 'NONE', #19287 ) ;
#811=CARTESIAN_POINT ( 'NONE',  ( 6.915128059151116610E-14, -5.777949443891209499E-13, 232.1412452697749984 ) ) ;
#849=DIRECTION ( 'NONE',  ( -0.9880370573969196046, 0.1542166437529879086, -5.551115123125782071E-14 ) ) ;
#858=CARTESIAN_POINT ( 'NONE',  ( -2.888061030901512893, 2.091444806125899891, -88.52261276243450538 ) ) ;
#934=ORIENTED_EDGE ( 'NONE', *, *, #11925, .F. ) ;
#992=FACE_OUTER_BOUND ( 'NONE', #10653, .T. ) ;
#1012=CARTESIAN_POINT ( 'NONE',  ( -3.873164306260329592, -2.119290473573849809, -95.69213427724059784 ) ) ;
#1037=DIRECTION ( 'NONE',  ( 0.1090476345695675503, 0.6986477033489619792, 0.7071067811865496822 ) ) ;
#1139=CARTESIAN_POINT ( 'NONE',  ( 2.127246859547380353, -2.914123423641564070, -88.52261276302716908 ) ) ;
#1292=CARTESIAN_POINT ( 'NONE',  ( -2.845423091905608715, -4.282740972715254557, -93.71305981297928156 ) ) ;
#1302=CARTESIAN_POINT ( 'NONE',  ( -0.5564057544751848106, -3.564787113710755850, -88.52261276293012315 ) ) ;
#1379=AXIS2_PLACEMENT_3D ( 'NONE', #11886, #4345, #16139 ) ;
#1462=FACE_OUTER_BOUND ( 'NONE', #30891, .T. ) ;
#1464=CARTESIAN_POINT ( 'NONE',  ( 0.4193002349296617859, -0.2844359550551249782, -98.16700801147769084 ) ) ;
#1522=VERTEX_POINT ( 'NONE', #12607 ) ;
#1543=APPLICATION_CONTEXT ( 'automotive_design' ) ;
#1584=CARTESIAN_POINT ( 'NONE',  ( 2.749352377422821903, -2.213834474264458230, 226.6412452697750837 ) ) ;
#1591=FACE_OUTER_BOUND ( 'NONE', #20842, .T. ) ;
#1603=CARTESIAN_POINT ( 'NONE',  ( -3.414938295376681587, -3.730152739507092363, -94.17120874162482380 ) ) ;
#1636=CARTESIAN_POINT ( 'NONE',  ( 3.556846951432204751, 0.09270462095633093258, -91.35798291625272327 ) ) ;
#1695=CARTESIAN_POINT ( 'NONE',  ( -1.317578093351431834, 0.7169295418041747858, 231.6412452697749984 ) ) ;
#1753=( NAMED_UNIT ( * ) PLANE_ANGLE_UNIT ( ) SI_UNIT ( $, .RADIAN. ) );
#1760=SURFACE_STYLE_USAGE ( .BOTH. , #16069 ) ;
#1823=CARTESIAN_POINT ( 'NONE',  ( 0.000000000000000000, 0.000000000000000000, 229.1412452697749984 ) ) ;
#1833=CARTESIAN_POINT ( 'NONE',  ( -3.388043077342722142, -1.111846212892217522, -88.52261276308685467 ) ) ;
#1841=EDGE_CURVE ( 'NONE', #11998, #790, #5415, .T. ) ;
#1914=CARTESIAN_POINT ( 'NONE',  ( 0.9930499629047704335, -5.067522214784211165, -93.52962329551429832 ) ) ;
#1926=CARTESIAN_POINT ( 'NONE',  ( -3.521042344302073079, -0.5632927345592675383, -88.52261276306772686 ) ) ;
#1961=CIRCLE ( 'NONE', #8463, 2.000000000000000000 ) ;
#1994=CARTESIAN_POINT ( 'NONE',  ( -2.914123423697624116, -2.127246859470591112, -88.52261276302716908 ) ) ;
#2014=B_SPLINE_CURVE_WITH_KNOTS ( 'NONE', 5,
 ( #9521, #12345, #12036, #12180, #7006, #19274, #16744, #403, #21791, #6843, #248, #24006, #14248, #9831, #21483 ),
 .UNSPECIFIED., .F., .F.,
 ( 6, 3, 3, 3, 6 ),
 ( 0.000000000000000000, 0.2499999999995511091, 0.4999999999991022182, 0.7499999999986531884, 1.000000000000000000 ),
 .UNSPECIFIED. ) ;
#2043=LINE ( 'NONE', #26264, #3448 ) ;
#2068=CARTESIAN_POINT ( 'NONE',  ( -2.595987296770100095, -16.63200279373747392, -109.8342699011499946 ) ) ;
#2079=CARTESIAN_POINT ( 'NONE',  ( -3.873164236031628516, -2.119290023631752007, -95.69213379017060106 ) ) ;
#2130=CARTESIAN_POINT ( 'NONE',  ( -5.000296138419098924, -9.340612320833740156, -88.85875473022500159 ) ) ;
#2186=AXIS2_PLACEMENT_3D ( 'NONE', #20936, #17927, #10709 ) ;
#2194=ORIENTED_EDGE ( 'NONE', *, *, #27275, .T. ) ;
#2278=DIRECTION ( 'NONE',  ( 0.000000000000000000, 0.000000000000000000, 1.000000000000000000 ) ) ;
#2331=ORIENTED_EDGE ( 'NONE', *, *, #18288, .T. ) ;
#2340=DIRECTION ( 'NONE',  ( 0.000000000000000000, 0.7113488923935510355, -0.7028390664230811380 ) ) ;
#2451=ORIENTED_EDGE ( 'NONE', *, *, #7138, .F. ) ;
#2493=LINE ( 'NONE', #12080, #28070 ) ;
#2513=FACE_OUTER_BOUND ( 'NONE', #8026, .T. ) ;
#2627=CARTESIAN_POINT ( 'NONE',  ( 0.000000000000000000, 0.000000000000000000, 0.000000000000000000 ) ) ;
#2647=CARTESIAN_POINT ( 'NONE',  ( -2.595987296770100095, -18.41037502479620969, -108.0771722350183381 ) ) ;
#2728=B_SPLINE_CURVE_WITH_KNOTS ( 'NONE', 3,
 ( #25200, #13227, #3804, #21110, #30554, #3957, #1914, #13555, #8983, #23163, #30706, #22844, #1292, #1603, #11193, #20792, #8823, #18426 ),
 .UNSPECIFIED., .F., .F.,
 ( 4, 2, 2, 2, 2, 2, 2, 2, 4 ),
 ( 0.000000000000000000, 0.1250000000000000278, 0.2500000000000000000, 0.3749999999999999445, 0.4999999999999999445, 0.6249999999999998890, 0.7499999999999998890, 0.8750000000000000000, 1.000000000000000000 ),
 .UNSPECIFIED. ) ;
#2792=EDGE_CURVE ( 'NONE', #6070, #11998, #10113, .T. ) ;
#2819=EDGE_LOOP ( 'NONE', ( #21416, #11954, #26297, #20006 ) ) ;
#2897=CARTESIAN_POINT ( 'NONE',  ( 0.3673706385115332318, 2.353674647662223673, -95.59336531685248417 ) ) ;
#3029=CARTESIAN_POINT ( 'NONE',  ( 4.239428892460699881E-14, 6.006117008548172241E-13, 232.1412452697749984 ) ) ;
#3044=COLOUR_RGB ( '', 0.66274510, 0.83137255, 0.94901961) ;
#3083=CARTESIAN_POINT ( 'NONE',  ( 3.458129700889219116, -0.5397582531354582214, 226.6412452697749984 ) ) ;
#3221=AXIS2_PLACEMENT_3D ( 'NONE', #1823, #27612, #30296 ) ;
#3263=AXIS2_PLACEMENT_3D ( 'NONE', #28518, #9318, #18920 ) ;
#3282=ORIENTED_EDGE ( 'NONE', *, *, #13953, .F. ) ;
#3334=CARTESIAN_POINT ( 'NONE',  ( 3.373344672752164985, -1.082959996301563477, -88.52261276311425320 ) ) ;
#3342=ORIENTED_EDGE ( 'NONE', *, *, #29821, .F. ) ;
#3352=CARTESIAN_POINT ( 'NONE',  ( 1.909260192367527864, 1.720838445342875778, -95.37004441182592984 ) ) ;
#3366=UNCERTAINTY_MEASURE_WITH_UNIT (LENGTH_MEASURE( 1.000000000000000082E-05 ), #11960, 'distance_accuracy_value', 'NONE');
#3370=EDGE_CURVE ( 'NONE', #13120, #12690, #2728, .T. ) ;
#3448=VECTOR ( 'NONE', #19022, 1000.000000000000114 ) ;
#3509=CARTESIAN_POINT ( 'NONE',  ( 2.899787796512155680, -2.016313622456245014, -96.83838116384302452 ) ) ;
#3643=CARTESIAN_POINT ( 'NONE',  ( 2.983143093411794400, -3.582908191650746588, -95.30338155897700858 ) ) ;
#3676=CONICAL_SURFACE ( 'NONE', #18756, 0.9999999999991029398, 0.7853981633970000820 ) ;
#3738=B_SPLINE_CURVE_WITH_KNOTS ( 'NONE', 3,
 ( #19763, #12513, #20648, #29347, #30246, #6010, #19916, #10898, #7789, #1464, #10323, #13241, #26837, #29503, #5433, #17082, #8359, #26682 ),
 .UNSPECIFIED., .F., .F.,
 ( 4, 2, 2, 2, 2, 2, 2, 2, 4 ),
 ( 0.000000000000000000, 0.1250000000000000000, 0.2500000000000000000, 0.3750000000000000000, 0.5000000000000000000, 0.6250000000000000000, 0.7500000000000000000, 0.8750000000000000000, 1.000000000000000000 ),
 .UNSPECIFIED. ) ;
#3754=LINE ( 'NONE', #10374, #21323 ) ;
#3790=CYLINDRICAL_SURFACE ( 'NONE', #2186, 3.500000000000000444 ) ;
#3804=CARTESIAN_POINT ( 'NONE',  ( 2.853188778929502512, -3.824801971133652945, -95.04434131334036806 ) ) ;
#3814=CARTESIAN_POINT ( 'NONE',  ( 1.976074114793839431, -0.3084332875059760948, 231.1412452697749984 ) ) ;
#3819=EDGE_CURVE ( 'NONE', #1522, #24923, #19473, .T. ) ;
#3835=CARTESIAN_POINT ( 'NONE',  ( 3.402386003322844132, -0.8968976485441944035, -94.01209571138487320 ) ) ;
#3871=EDGE_CURVE ( 'NONE', #7336, #27477, #26021, .T. ) ;
#3877=CARTESIAN_POINT ( 'NONE',  ( 2.888061030912462801, -2.091444806055747563, -88.52261276308685467 ) ) ;
#3953=ORIENTED_EDGE ( 'NONE', *, *, #24379, .T. ) ;
#3957=CARTESIAN_POINT ( 'NONE',  ( 1.404941437947275551, -4.946154300792606762, -93.71305981298847598 ) ) ;
#4081=ORIENTED_EDGE ( 'NONE', *, *, #13374, .F. ) ;
#4272=DIRECTION ( 'NONE',  ( 0.1090476345695675503, 0.6986477033489619792, 0.7071067811865496822 ) ) ;
#4285=CARTESIAN_POINT ( 'NONE',  ( -3.729856948807544814, -3.301783456504468806, -94.54588698005633773 ) ) ;
#4345=DIRECTION ( 'NONE',  ( 0.000000000000000000, 0.000000000000000000, 1.000000000000000000 ) ) ;
#4438=EDGE_CURVE ( 'NONE', #21319, #22703, #17075, .T. ) ;
#4449=CIRCLE ( 'NONE', #19522, 2.500000000105230491 ) ;
#4694=DIRECTION ( 'NONE',  ( 0.000000000000000000, 0.7113488923935510355, -0.7028390664230811380 ) ) ;
#4748=AXIS2_PLACEMENT_3D ( 'NONE', #10840, #17737, #30020 ) ;
#4791=CARTESIAN_POINT ( 'NONE',  ( -2.595987296758533791, -16.63200279366337497, -109.8342699012249994 ) ) ;
#4872=DIRECTION ( 'NONE',  ( -0.1090476345695678556, -0.6986477033489640887, -0.7071067811865475727 ) ) ;
#4882=SHAPE_REPRESENTATION_RELATIONSHIP ( 'NONE' , 'NONE' ,  #17403, #20440 ) ;
#4969=ADVANCED_FACE ( 'NONE', ( #992 ), #18850, .T. ) ;
#5038=( NAMED_UNIT ( * ) SI_UNIT ( $, .STERADIAN. ) SOLID_ANGLE_UNIT ( ) );
#5060=EDGE_CURVE ( 'NONE', #12690, #6489, #5392, .T. ) ;
#5143=DIRECTION ( 'NONE',  ( -0.1090476345695678556, -0.6986477033489640887, -0.7071067811865475727 ) ) ;
#5219=ORIENTED_EDGE ( 'NONE', *, *, #27942, .T. ) ;
#5240=DIRECTION ( 'NONE',  ( -0.1090476345695678695, -0.6986477033489640887, -0.7071067811865474617 ) ) ;
#5261=CARTESIAN_POINT ( 'NONE',  ( 2.914123423709013228, 2.127246859543532764, -88.52261276242110455 ) ) ;
#5294=AXIS2_PLACEMENT_3D ( 'NONE', #25055, #22549, #24598 ) ;
#5392=LINE ( 'NONE', #11516, #26408 ) ;
#5409=CARTESIAN_POINT ( 'NONE',  ( -2.113314637130261353, 3.003384554638903303, -91.89588846697527913 ) ) ;
#5415=LINE ( 'NONE', #5722, #31091 ) ;
#5433=CARTESIAN_POINT ( 'NONE',  ( 2.798846661298902916, -1.899199287238114930, -96.93852766386672215 ) ) ;
#5457=ORIENTED_EDGE ( 'NONE', *, *, #27275, .F. ) ;
#5562=CARTESIAN_POINT ( 'NONE',  ( -0.5632927345598660596, 3.521042344314967210, -88.52261276241718235 ) ) ;
#5657=CIRCLE ( 'NONE', #14207, 2.000000000000000000 ) ;
#5688=ORIENTED_EDGE ( 'NONE', *, *, #25620, .T. ) ;
#5699=CARTESIAN_POINT ( 'NONE',  ( 2.781964183363350607, -2.771187371452367376, -92.88964426498925775 ) ) ;
#5718=CARTESIAN_POINT ( 'NONE',  ( -0.7489034454876208891, 2.331869397845270253, -95.48173244568418738 ) ) ;
#5722=CARTESIAN_POINT ( 'NONE',  ( -3.458129700889219116, 0.5397582531354577773, -85.94068374672499999 ) ) ;
#5867=CARTESIAN_POINT ( 'NONE',  ( 3.401975299758845050, 1.201107343883199841, -91.64589571366730070 ) ) ;
#5892=AXIS2_PLACEMENT_3D ( 'NONE', #22649, #8622, #10540 ) ;
#5924=ORIENTED_EDGE ( 'NONE', *, *, #5060, .T. ) ;
#5996=DIRECTION ( 'NONE',  ( 0.9880370573969196046, -0.1542166437529877976, 0.000000000000000000 ) ) ;
#6008=CARTESIAN_POINT ( 'NONE',  ( 1.827447710699809269, -4.834880234507621388, -93.88815951138720095 ) ) ;
#6010=CARTESIAN_POINT ( 'NONE',  ( -2.235010648674410128, -0.3719431525293064866, -97.67120874165279076 ) ) ;
#6070=VERTEX_POINT ( 'NONE', #24752 ) ;
#6162=CARTESIAN_POINT ( 'NONE',  ( 3.195834452880789822, -1.520253115373796149, -90.91470530330329325 ) ) ;
#6237=AXIS2_PLACEMENT_3D ( 'NONE', #25466, #16012, #28277 ) ;
#6240=UNCERTAINTY_MEASURE_WITH_UNIT (LENGTH_MEASURE( 1.000000000000000082E-05 ), #17142, 'distance_accuracy_value', 'NONE');
#6300=MECHANICAL_DESIGN_GEOMETRIC_PRESENTATION_REPRESENTATION('',(#23411),#24903);
#6377=CYLINDRICAL_SURFACE ( 'NONE', #3221, 2.000000000000000000 ) ;
#6465=SURFACE_STYLE_FILL_AREA ( #18424 ) ;
#6466=DIRECTION ( 'NONE',  ( 0.000000000000000000, -0.7113488923935513686, 0.7028390664230806939 ) ) ;
#6478=CARTESIAN_POINT ( 'NONE',  ( -3.444197479758565272, 0.6290193758906742483, -91.21022354329026882 ) ) ;
#6489=VERTEX_POINT ( 'NONE', #17032 ) ;
#6496=DIRECTION ( 'NONE',  ( 0.000000000000000000, 0.000000000000000000, 1.000000000000000000 ) ) ;
#6542=CARTESIAN_POINT ( 'NONE',  ( -0.5564057544751848106, -3.564787113710755850, -88.52261276293012315 ) ) ;
#6566=CARTESIAN_POINT ( 'NONE',  ( -1.505510951065242020, -9.645525760189025632, -102.7632020892250040 ) ) ;
#6601=CARTESIAN_POINT ( 'NONE',  ( 0.3786683407719231842, -3.509503079120984026, 226.6412452697750268 ) ) ;
#6604=AXIS2_PLACEMENT_3D ( 'NONE', #26883, #29701, #25136 ) ;
#6632=PRODUCT_DEFINITION_SHAPE ( 'NONE', 'NONE',  #15768 ) ;
#6649=CARTESIAN_POINT ( 'NONE',  ( -1.976074114793839431, 0.3084332875059758727, 229.1412452697749984 ) ) ;
#6677=DIRECTION ( 'NONE',  ( 0.000000000000000000, 0.000000000000000000, 1.000000000000000000 ) ) ;
#6685=ADVANCED_FACE ( 'NONE', ( #20318 ), #29918, .T. ) ;
#6696=CARTESIAN_POINT ( 'NONE',  ( -3.521042344302073079, -0.5632927345592675383, -88.52261276306772686 ) ) ;
#6728=ORIENTED_EDGE ( 'NONE', *, *, #24020, .F. ) ;
#6843=CARTESIAN_POINT ( 'NONE',  ( 2.091444806099476583, 2.888061030883168456, -88.52261276238974119 ) ) ;
#6908=CARTESIAN_POINT ( 'NONE',  ( 3.227294851203073023, -1.430228209132706318, 226.6412452697750268 ) ) ;
#6947=CARTESIAN_POINT ( 'NONE',  ( -3.458129700886692248, 0.5397582531516398330, -88.52261276316077954 ) ) ;
#6974=ORIENTED_EDGE ( 'NONE', *, *, #26867, .F. ) ;
#7006=CARTESIAN_POINT ( 'NONE',  ( -2.127246859535990353, 2.914123423714512384, -88.52261276242110455 ) ) ;
#7024=DIRECTION ( 'NONE',  ( -0.9880370573969197157, 0.1542166437529879364, 0.000000000000000000 ) ) ;
#7138=EDGE_CURVE ( 'NONE', #27710, #18256, #23708, .T. ) ;
#7241=SURFACE_STYLE_FILL_AREA ( #16988 ) ;
#7336=VERTEX_POINT ( 'NONE', #21962 ) ;
#7456=DIRECTION ( 'NONE',  ( 0.000000000000000000, -0.7113488923935513686, 0.7028390664230806939 ) ) ;
#7507=ORIENTED_EDGE ( 'NONE', *, *, #13732, .F. ) ;
#7568=DIRECTION ( 'NONE',  ( 0.9880370573969197157, -0.1542166437529878531, -1.665334536939228724E-13 ) ) ;
#7614=CARTESIAN_POINT ( 'NONE',  ( -0.5493605121539751890, 3.610303475240396409, -92.12187520236776095 ) ) ;
#7738=ORIENTED_EDGE ( 'NONE', *, *, #13231, .F. ) ;
#7768=CARTESIAN_POINT ( 'NONE',  ( -3.458129700890608671, 0.5397582531265487926, -88.52261276240527366 ) ) ;
#7789=CARTESIAN_POINT ( 'NONE',  ( -0.4860360036921328453, -0.1431275748294068006, -98.16700801147820243 ) ) ;
#7892=ORIENTED_EDGE ( 'NONE', *, *, #24020, .T. ) ;
#7916=CARTESIAN_POINT ( 'NONE',  ( -3.376316311743029708, -1.036715029292714529, -96.83838116384302452 ) ) ;
#8026=EDGE_LOOP ( 'NONE', ( #29944, #22146, #23630, #24667 ) ) ;
#8030=VERTEX_POINT ( 'NONE', #28457 ) ;
#8070=CARTESIAN_POINT ( 'NONE',  ( 1.609514238142041975, 3.181902231760902477, -88.52261276241718235 ) ) ;
#8202=CARTESIAN_POINT ( 'NONE',  ( 1.125778434080668244, -3.298781954526681215, -90.35662574872537789 ) ) ;
#8220=CARTESIAN_POINT ( 'NONE',  ( -3.373344672752120132, 1.082959996301855021, -88.52261276241732446 ) ) ;
#8235=CIRCLE ( 'NONE', #26857, 1.500000000000000222 ) ;
#8270=ORIENTED_EDGE ( 'NONE', *, *, #24379, .F. ) ;
#8357=CARTESIAN_POINT ( 'NONE',  ( 2.546247159447640573, -4.281382049667992185, -94.54588698005632352 ) ) ;
#8359=CARTESIAN_POINT ( 'NONE',  ( 3.093055152476274383, -2.878722282980446412, -96.01609449156637766 ) ) ;
#8463=AXIS2_PLACEMENT_3D ( 'NONE', #21347, #30944, #7024 ) ;
#8514=CARTESIAN_POINT ( 'NONE',  ( -0.8084728434465671132, -5.179733586367765596, -93.14092889888253524 ) ) ;
#8536=ORIENTED_EDGE ( 'NONE', *, *, #13953, .T. ) ;
#8622=DIRECTION ( 'NONE',  ( 0.000000000000000000, 0.000000000000000000, 1.000000000000000000 ) ) ;
#8626=CARTESIAN_POINT ( 'NONE',  ( -3.873164306258084277, -2.119290473559455101, -95.69213427732501032 ) ) ;
#8654=ADVANCED_FACE ( 'NONE', ( #17501 ), #16468, .T. ) ;
#8674=CARTESIAN_POINT ( 'NONE',  ( -2.091444806098883280, -2.888061030879386593, -88.52261276293990022 ) ) ;
#8803=CARTESIAN_POINT ( 'NONE',  ( -3.097451722119552997, -1.692897434402192092, 226.6412452697750268 ) ) ;
#8821=FILL_AREA_STYLE_COLOUR ( '', #3044 ) ;
#8823=CARTESIAN_POINT ( 'NONE',  ( -3.923124363200321429, -2.439375170321697706, -95.36817406305493705 ) ) ;
#8831=CARTESIAN_POINT ( 'NONE',  ( -3.933116308366643388, -2.503391685379829923, -95.30338155897700858 ) ) ;
#8934=ORIENTED_EDGE ( 'NONE', *, *, #27309, .F. ) ;
#8963=CARTESIAN_POINT ( 'NONE',  ( 3.458129700889219116, -0.5397582531354582214, 226.6412452697749984 ) ) ;
#8983=CARTESIAN_POINT ( 'NONE',  ( -0.3440332070342348447, -5.174969878487565289, -93.21726054315809051 ) ) ;
#8993=CARTESIAN_POINT ( 'NONE',  ( -3.666003079838183965, -0.7920474239279197137, -93.44355375713804790 ) ) ;
#9151=ORIENTED_EDGE ( 'NONE', *, *, #30591, .F. ) ;
#9181=ORIENTED_EDGE ( 'NONE', *, *, #17382, .T. ) ;
#9268=CARTESIAN_POINT ( 'NONE',  ( -1.430228209136418238, -3.227294851201703896, 226.6412452697749700 ) ) ;
#9284=( NAMED_UNIT ( * ) SI_UNIT ( $, .STERADIAN. ) SOLID_ANGLE_UNIT ( ) );
#9304=CARTESIAN_POINT ( 'NONE',  ( -3.635410520752169194, -1.296028149944132402, -93.15928300860232980 ) ) ;
#9315=DIRECTION ( 'NONE',  ( -0.1090476345695678556, -0.6986477033489640887, -0.7071067811865475727 ) ) ;
#9318=DIRECTION ( 'NONE',  ( 0.1090476345695682997, 0.6986477033489653099, 0.7071067811865462405 ) ) ;
#9521=CARTESIAN_POINT ( 'NONE',  ( -3.458129700889219116, 0.5397582531354577773, -88.52261276322501260 ) ) ;
#9539=DIRECTION ( 'NONE',  ( 0.7757560252248331123, 0.3849708941249066485, 0.5000000000040377701 ) ) ;
#9754=ORIENTED_EDGE ( 'NONE', *, *, #17382, .F. ) ;
#9765=AXIS2_PLACEMENT_3D ( 'NONE', #26964, #15009, #7456 ) ;
#9823=DIRECTION ( 'NONE',  ( -0.9880370573969197157, 0.1542166437529879364, 0.000000000000000000 ) ) ;
#9827=DIRECTION ( 'NONE',  ( 0.1542166437529880196, 0.9880370573969197157, 0.000000000000000000 ) ) ;
#9831=CARTESIAN_POINT ( 'NONE',  ( 3.542914729026319876, 0.003443490030938245461, -88.52261276241732446 ) ) ;
#9902=CARTESIAN_POINT ( 'NONE',  ( -1.505510951065242020, -9.645525760189025632, -102.7632020892250040 ) ) ;
#10031=EDGE_LOOP ( 'NONE', ( #24386, #15326, #16087, #22796 ) ) ;
#10113=B_SPLINE_CURVE_WITH_KNOTS ( 'NONE', 5,
 ( #23706, #25444, #13944, #3877, #28253, #25754, #20712, #6542, #13466, #16140, #1994, #1833, #6696, #16296, #23558 ),
 .UNSPECIFIED., .F., .F.,
 ( 6, 3, 3, 3, 6 ),
 ( 0.000000000000000000, 0.2500000000035760284, 0.4999999999999331091, 0.7500000000052684523, 1.000000000000000000 ),
 .UNSPECIFIED. ) ;
#10140=ADVANCED_FACE ( 'NONE', ( #14257, #23402 ), #11426, .T. ) ;
#10141=CARTESIAN_POINT ( 'NONE',  ( 3.056341819332166310, -2.413956206206734123, -96.46963879144223597 ) ) ;
#10157=CARTESIAN_POINT ( 'NONE',  ( -0.1258946531760308241, -17.01754440315029271, -109.8342699011357126 ) ) ;
#10301=CARTESIAN_POINT ( 'NONE',  ( -2.127246859535990353, 2.914123423714512384, -88.52261276242110455 ) ) ;
#10323=CARTESIAN_POINT ( 'NONE',  ( 0.8618564855135213421, -0.4187060996060523732, -98.10259367259374130 ) ) ;
#10374=CARTESIAN_POINT ( 'NONE',  ( 3.458129700889219116, -0.5397582531354573332, -85.94068374672499999 ) ) ;
#10402=EDGE_LOOP ( 'NONE', ( #19086, #14949, #19237, #13148 ) ) ;
#10450=CARTESIAN_POINT ( 'NONE',  ( -1.670339710860670568, -0.1901198163082873371, -97.93793859254537892 ) ) ;
#10540=DIRECTION ( 'NONE',  ( -0.9880370573969197157, 0.1542166437529879364, 0.000000000000000000 ) ) ;
#10585=CARTESIAN_POINT ( 'NONE',  ( -1.595582016994381069, -3.092641108896711177, -90.29857220542305640 ) ) ;
#10601=CARTESIAN_POINT ( 'NONE',  ( -3.513873398455594987, 0.1826188577267222057, -94.01209571138487320 ) ) ;
#10653=EDGE_LOOP ( 'NONE', ( #26587, #26440, #2451, #8270 ) ) ;
#10667=VECTOR ( 'NONE', #229, 1000.000000000000114 ) ;
#10709=DIRECTION ( 'NONE',  ( -0.9880370573969196046, 0.1542166437529879086, 0.000000000000000000 ) ) ;
#10732=CARTESIAN_POINT ( 'NONE',  ( 2.035903620463144659, -3.499342391980986733, -92.40868836340082737 ) ) ;
#10840=CARTESIAN_POINT ( 'NONE',  ( 2.114229738758179432E-14, 3.003144111683443606E-13, 231.6412452697749984 ) ) ;
#10896=CARTESIAN_POINT ( 'NONE',  ( -0.5424735333374979263, -3.475525990910468987, -90.24054733466465450 ) ) ;
#10898=CARTESIAN_POINT ( 'NONE',  ( -0.9484597805798516967, -0.1361449379680841898, -98.10259367259483554 ) ) ;
#10902=CARTESIAN_POINT ( 'NONE',  ( 2.114229738758179432E-14, 3.003144111683443606E-13, 231.6412452697749984 ) ) ;
#10934=DIRECTION ( 'NONE',  ( 0.9880370573969197157, -0.1542166437529880196, 2.958228394580000263E-31 ) ) ;
#11054=CARTESIAN_POINT ( 'NONE',  ( 3.043095165746811048, -3.198806529902668672, -95.69213379017060106 ) ) ;
#11103=FACE_OUTER_BOUND ( 'NONE', #24122, .T. ) ;
#11193=CARTESIAN_POINT ( 'NONE',  ( -3.628915872023533495, -3.418898166067736000, -94.44574089075830159 ) ) ;
#11225=CARTESIAN_POINT ( 'NONE',  ( 3.103047163856258006, -2.814705343703844065, -96.08088653434137427 ) ) ;
#11333=CARTESIAN_POINT ( 'NONE',  ( -3.458129700889219116, 0.5397582531354577773, 226.6412452697749984 ) ) ;
#11426=PLANE ( 'NONE',  #1379 ) ;
#11442=CARTESIAN_POINT ( 'NONE',  ( -1.482055586095422983, 0.2313249656292047651, 231.6412452697749984 ) ) ;
#11455=FACE_OUTER_BOUND ( 'NONE', #22678, .T. ) ;
#11516=CARTESIAN_POINT ( 'NONE',  ( -4.963640651960628425, -9.105767507093087687, -102.7632020892250040 ) ) ;
#11517=CARTESIAN_POINT ( 'NONE',  ( -3.388043077342722142, -1.111846212892217522, -88.52261276308685467 ) ) ;
#11555=VECTOR ( 'NONE', #16299, 1000.000000000000114 ) ;
#11640=CARTESIAN_POINT ( 'NONE',  ( -3.509503079120555036, -0.3786683407750112695, 226.6412452697750268 ) ) ;
#11671=CARTESIAN_POINT ( 'NONE',  ( -3.886410967837877539, -2.904140848474241920, -94.91462932778338768 ) ) ;
#11689=B_SPLINE_CURVE_WITH_KNOTS ( 'NONE', 3,
 ( #11333, #21090, #11640, #21240, #8803, #30837, #23143, #9268, #28004, #19028, #6601, #18874, #20768, #28471, #1584, #6908, #16510, #8963 ),
 .UNSPECIFIED., .F., .F.,
 ( 4, 2, 2, 2, 2, 2, 2, 2, 4 ),
 ( 0.000000000000000000, 0.1250000000000000555, 0.2500000000000001110, 0.3750000000000001665, 0.5000000000000001110, 0.6250000000000001110, 0.7500000000000001110, 0.8750000000000000000, 1.000000000000000000 ),
 .UNSPECIFIED. ) ;
#11751=EDGE_CURVE ( 'NONE', #6489, #8030, #17963, .T. ) ;
#11831=CARTESIAN_POINT ( 'NONE',  ( -3.374110856211531395, -1.022585090133552033, -90.77455165165939377 ) ) ;
#11863=DIRECTION ( 'NONE',  ( -0.9880370573969196046, 0.1542166437529879086, 0.000000000000000000 ) ) ;
#11873=EDGE_CURVE ( 'NONE', #24923, #22531, #4449, .T. ) ;
#11886=CARTESIAN_POINT ( 'NONE',  ( 0.000000000000000000, 0.000000000000000000, 226.6412452697749984 ) ) ;
#11925=EDGE_CURVE ( 'NONE', #6489, #1522, #2493, .T. ) ;
#11954=ORIENTED_EDGE ( 'NONE', *, *, #29436, .F. ) ;
#11960=( LENGTH_UNIT ( ) NAMED_UNIT ( * ) SI_UNIT ( .MILLI., .METRE. ) );
#11977=CARTESIAN_POINT ( 'NONE',  ( -3.589938226060418902, -0.3047141992580486569, -93.72782450567366652 ) ) ;
#11998=VERTEX_POINT ( 'NONE', #27629 ) ;
#12036=CARTESIAN_POINT ( 'NONE',  ( -3.181902231748757526, 1.609514238137835118, -88.52261276242234089 ) ) ;
#12080=CARTESIAN_POINT ( 'NONE',  ( -5.945069363104309446, -15.39359683734632611, -109.1271631200178547 ) ) ;
#12180=CARTESIAN_POINT ( 'NONE',  ( -2.888061030901512893, 2.091444806125899891, -88.52261276243450538 ) ) ;
#12255=VECTOR ( 'NONE', #6496, 1000.000000000000000 ) ;
#12301=CARTESIAN_POINT ( 'NONE',  ( 1.976074114793839431, -0.3084332875059760948, 229.1412452697749984 ) ) ;
#12345=CARTESIAN_POINT ( 'NONE',  ( -3.373344672752120132, 1.082959996301855021, -88.52261276241732446 ) ) ;
#12464=CONICAL_SURFACE ( 'NONE', #14974, 2.500000000105231823, 0.7853981633974348453 ) ;
#12490=ORIENTED_EDGE ( 'NONE', *, *, #30591, .T. ) ;
#12492=CARTESIAN_POINT ( 'NONE',  ( 3.521042344302120153, 0.5632927345595589719, -88.52261276242234089 ) ) ;
#12513=CARTESIAN_POINT ( 'NONE',  ( -3.823204249305973690, -1.799205776751950703, -96.01609449157885479 ) ) ;
#12607=CARTESIAN_POINT ( 'NONE',  ( -5.066079940368577006, -16.24646118435289566, -109.8342699011357126 ) ) ;
#12622=DIRECTION ( 'NONE',  ( -4.250489863289427893E-14, -6.005940811918155400E-13, -1.000000000000000000 ) ) ;
#12684=ORIENTED_EDGE ( 'NONE', *, *, #3370, .T. ) ;
#12690=VERTEX_POINT ( 'NONE', #8626 ) ;
#12788=CARTESIAN_POINT ( 'NONE',  ( 1.952618749817809141, -10.18528401336400435, -102.7632020892250040 ) ) ;
#12808=CARTESIAN_POINT ( 'NONE',  ( -3.167970009343080484, 1.698775369061893636, -91.50574204942923018 ) ) ;
#12821=CIRCLE ( 'NONE', #3263, 3.500000000000002220 ) ;
#12839=COLOUR_RGB ( '', 0.66274510, 0.83137255, 0.94901961) ;
#12943=CARTESIAN_POINT ( 'NONE',  ( -1.871333206045247888, -4.859327160240900056, -93.29359154310911606 ) ) ;
#12959=CARTESIAN_POINT ( 'NONE',  ( 2.928055646114741783, 2.216507990467923683, -91.89588846697527913 ) ) ;
#13020=CARTESIAN_POINT ( 'NONE',  ( 3.466821295769682159E-14, -2.890242878314739659E-13, 231.6412452697749984 ) ) ;
#13057=FACE_OUTER_BOUND ( 'NONE', #28068, .T. ) ;
#13106=CARTESIAN_POINT ( 'NONE',  ( 3.534974566707796306, 0.6525538654836177122, -91.50574204942923018 ) ) ;
#13120=VERTEX_POINT ( 'NONE', #18662 ) ;
#13130=CARTESIAN_POINT ( 'NONE',  ( 1.482055586095336386, -0.2313249656297586831, 231.6412452697749984 ) ) ;
#13148=ORIENTED_EDGE ( 'NONE', *, *, #22641, .T. ) ;
#13227=CARTESIAN_POINT ( 'NONE',  ( 2.993135038577686036, -3.518891676577371896, -95.36817406306990108 ) ) ;
#13231=EDGE_CURVE ( 'NONE', #18256, #13982, #1961, .T. ) ;
#13239=CARTESIAN_POINT ( 'NONE',  ( 0.5772249557075271875, -3.431781221450775909, -90.29857220542305640 ) ) ;
#13241=CARTESIAN_POINT ( 'NONE',  ( 1.660040334269103246, -0.7942402406998696485, -97.85464525912325939 ) ) ;
#13345=PRODUCT_DEFINITION_FORMATION_WITH_SPECIFIED_SOURCE ( 'ANY', '', #20959, .NOT_KNOWN. ) ;
#13374=EDGE_CURVE ( 'NONE', #24923, #13901, #576, .T. ) ;
#13448=DIRECTION ( 'NONE',  ( 0.000000000000000000, 0.7113488923935522568, -0.7028390664230799167 ) ) ;
#13466=CARTESIAN_POINT ( 'NONE',  ( -1.609514238130545838, -3.181902231687246285, -88.52261276296684400 ) ) ;
#13494=DIRECTION ( 'NONE',  ( 0.9880370573969196046, -0.1542166437529880751, 0.000000000000000000 ) ) ;
#13505=ORIENTED_EDGE ( 'NONE', *, *, #27343, .F. ) ;
#13555=CARTESIAN_POINT ( 'NONE',  ( 0.1183905698532920631, -5.181952515350124244, -93.28167488204269375 ) ) ;
#13566=CARTESIAN_POINT ( 'NONE',  ( -2.077512584961602293, -2.798799908081698540, -90.35662574872537789 ) ) ;
#13640=ADVANCED_FACE ( 'NONE', ( #17045 ), #19412, .T. ) ;
#13732=EDGE_CURVE ( 'NONE', #26662, #790, #20552, .T. ) ;
#13793=CIRCLE ( 'NONE', #25873, 10.00564797610000056 ) ;
#13901=VERTEX_POINT ( 'NONE', #30831 ) ;
#13944=CARTESIAN_POINT ( 'NONE',  ( 3.181902231748806376, -1.609514238137543796, -88.52261276306772686 ) ) ;
#13953=EDGE_CURVE ( 'NONE', #14643, #13982, #2043, .T. ) ;
#13982=VERTEX_POINT ( 'NONE', #3814 ) ;
#14015=DIRECTION ( 'NONE',  ( 0.000000000000000000, 0.000000000000000000, 1.000000000000000000 ) ) ;
#14017=ORIENTED_EDGE ( 'NONE', *, *, #3871, .F. ) ;
#14207=AXIS2_PLACEMENT_3D ( 'NONE', #28703, #6677, #26350 ) ;
#14248=CARTESIAN_POINT ( 'NONE',  ( 3.521042344302120153, 0.5632927345595589719, -88.52261276242234089 ) ) ;
#14257=FACE_BOUND ( 'NONE', #23067, .T. ) ;
#14270=AXIS2_PLACEMENT_3D ( 'NONE', #9902, #4872, #29091 ) ;
#14289=AXIS2_PLACEMENT_3D ( 'NONE', #30133, #1037, #13448 ) ;
#14415=CARTESIAN_POINT ( 'NONE',  ( -349323.8516741809435, 54523.81728493721312, -353320.2493477302487 ) ) ;
#14540=VECTOR ( 'NONE', #9539, 1000.000000000000114 ) ;
#14561=ORIENTED_EDGE ( 'NONE', *, *, #29436, .T. ) ;
#14643=VERTEX_POINT ( 'NONE', #13130 ) ;
#14766=DIRECTION ( 'NONE',  ( 0.07710832187649481473, -0.008981096902548890704, 0.9969822699505833663 ) ) ;
#14871=CARTESIAN_POINT ( 'NONE',  ( -3.045581262757260266, 1.082242280537820678, -94.56600524946087205 ) ) ;
#14949=ORIENTED_EDGE ( 'NONE', *, *, #27942, .F. ) ;
#14974=AXIS2_PLACEMENT_3D ( 'NONE', #2068, #4272, #6466 ) ;
#15009=DIRECTION ( 'NONE',  ( 0.1090476345695675503, 0.6986477033489619792, 0.7071067811865496822 ) ) ;
#15055=ADVANCED_FACE ( 'NONE', ( #21259 ), #12464, .T. ) ;
#15078=CYLINDRICAL_SURFACE ( 'NONE', #6604, 2.000000000000000000 ) ;
#15163=CARTESIAN_POINT ( 'NONE',  ( 0.5564057544863512117, 3.564787113782302619, -88.52261276243972077 ) ) ;
#15306=CARTESIAN_POINT ( 'NONE',  ( 0.8402705472655720431, -5.127977335047565255, -93.44632962453067648 ) ) ;
#15324=CARTESIAN_POINT ( 'NONE',  ( -0.02159632328769568732, -0.1383635851000819539, -98.24333933864600965 ) ) ;
#15326=ORIENTED_EDGE ( 'NONE', *, *, #27343, .T. ) ;
#15477=CARTESIAN_POINT ( 'NONE',  ( 3.230522845497924234, 0.1026436873742902073, -94.56600524946087205 ) ) ;
#15492=ORIENTED_EDGE ( 'NONE', *, *, #13732, .T. ) ;
#15570=ORIENTED_EDGE ( 'NONE', *, *, #13374, .T. ) ;
#15586=( LENGTH_UNIT ( ) NAMED_UNIT ( * ) SI_UNIT ( .MILLI., .METRE. ) );
#15597=EDGE_LOOP ( 'NONE', ( #22412, #24690, #12490, #29169, #3342 ) ) ;
#15606=CARTESIAN_POINT ( 'NONE',  ( 0.5632927345713620859, -3.521042344241311017, -88.52261276296684400 ) ) ;
#15724=DIRECTION ( 'NONE',  ( 0.000000000000000000, 0.000000000000000000, 1.000000000000000000 ) ) ;
#15744=( NAMED_UNIT ( * ) SI_UNIT ( $, .STERADIAN. ) SOLID_ANGLE_UNIT ( ) );
#15764=CARTESIAN_POINT ( 'NONE',  ( -1.609514238130545838, -3.181902231687246285, -88.52261276296684400 ) ) ;
#15768=PRODUCT_DEFINITION ( 'UNKNOWN', '', #13345, #23564 ) ;
#15828=VECTOR ( 'NONE', #26525, 1000.000000000000000 ) ;
#15862=CYLINDRICAL_SURFACE ( 'NONE', #22351, 3.500000000000000444 ) ;
#15923=CARTESIAN_POINT ( 'NONE',  ( 3.387276893882220641, -0.9936988735501727232, -91.06246442329681656 ) ) ;
#16012=DIRECTION ( 'NONE',  ( 0.000000000000000000, 0.000000000000000000, 1.000000000000000000 ) ) ;
#16064=AXIS2_PLACEMENT_3D ( 'NONE', #27098, #17939, #5996 ) ;
#16069=SURFACE_SIDE_STYLE ('',( #6465 ) ) ;
#16080=CARTESIAN_POINT ( 'NONE',  ( -2.900191202563959791, -2.037985736696075634, -90.52455892065360388 ) ) ;
#16087=ORIENTED_EDGE ( 'NONE', *, *, #11751, .F. ) ;
#16101=CARTESIAN_POINT ( 'NONE',  ( 3.472061923294214036, -0.4504971222157764243, -91.21022378307108625 ) ) ;
#16139=DIRECTION ( 'NONE',  ( -0.9880370573969196046, 0.1542166437529879364, 0.000000000000000000 ) ) ;
#16140=CARTESIAN_POINT ( 'NONE',  ( -2.091444806098883280, -2.888061030879386593, -88.52261276293990022 ) ) ;
#16296=CARTESIAN_POINT ( 'NONE',  ( -3.542914729026271914, -0.003443490030646811917, -88.52261276311425320 ) ) ;
#16299=DIRECTION ( 'NONE',  ( -0.6986477033484088661, 0.1090476345698817712, -0.7071067811870476172 ) ) ;
#16370=SURFACE_STYLE_USAGE ( .BOTH. , #23936 ) ;
#16387=DIRECTION ( 'NONE',  ( -0.1090476345695678556, -0.6986477033489640887, -0.7071067811865474617 ) ) ;
#16412=ORIENTED_EDGE ( 'NONE', *, *, #3370, .F. ) ;
#16468=CONICAL_SURFACE ( 'NONE', #30027, 0.9999999999991034949, 0.7853981633970000820 ) ;
#16510=CARTESIAN_POINT ( 'NONE',  ( 3.387192064160615690, -0.9942423616359961080, 226.6412452697750268 ) ) ;
#16552=DIRECTION ( 'NONE',  ( 0.000000000000000000, 0.7113488923935510355, -0.7028390664230811380 ) ) ;
#16598=EDGE_CURVE ( 'NONE', #13120, #13901, #24600, .T. ) ;
#16698=ADVANCED_FACE ( 'NONE', ( #1462 ), #31022, .T. ) ;
#16724=AXIS2_PLACEMENT_3D ( 'NONE', #13020, #17729, #20257 ) ;
#16744=CARTESIAN_POINT ( 'NONE',  ( -0.5632927345598660596, 3.521042344314967210, -88.52261276241718235 ) ) ;
#16787=AXIS2_PLACEMENT_3D ( 'NONE', #26654, #21942, #9823 ) ;
#16839=AXIS2_PLACEMENT_3D ( 'NONE', #2130, #244, #9827 ) ;
#16988=FILL_AREA_STYLE ('',( #21885 ) ) ;
#16994=PRESENTATION_STYLE_ASSIGNMENT (( #1760 ) ) ;
#16997=AXIS2_PLACEMENT_3D ( 'NONE', #18692, #18854, #25946 ) ;
#17018=ORIENTED_EDGE ( 'NONE', *, *, #22849, .F. ) ;
#17032=CARTESIAN_POINT ( 'NONE',  ( -5.945069363104310334, -15.39359683734633677, -109.1271631200178689 ) ) ;
#17045=FACE_OUTER_BOUND ( 'NONE', #23272, .T. ) ;
#17075=LINE ( 'NONE', #21657, #15828 ) ;
#17082=CARTESIAN_POINT ( 'NONE',  ( 3.052989692426276491, -2.544715063274864519, -96.33992724129673491 ) ) ;
#17116=LINE ( 'NONE', #2647, #26359 ) ;
#17142=( LENGTH_UNIT ( ) NAMED_UNIT ( * ) SI_UNIT ( .MILLI., .METRE. ) );
#17207=CARTESIAN_POINT ( 'NONE',  ( -1.756770791141829546, 0.9559060557399279290, 231.1412452697749984 ) ) ;
#17211=CARTESIAN_POINT ( 'NONE',  ( 1.041264040880410136, -0.4587700011719486604, -98.09067668424567898 ) ) ;
#17221=AXIS2_PLACEMENT_3D ( 'NONE', #23335, #20964, #26002 ) ;
#17225=UNCERTAINTY_MEASURE_WITH_UNIT (LENGTH_MEASURE( 1.000000000000000082E-05 ), #15586, 'distance_accuracy_value', 'NONE');
#17382=EDGE_CURVE ( 'NONE', #27477, #7336, #5657, .T. ) ;
#17403=SHAPE_REPRESENTATION ( 'Plunger Rod', ( #17722 ), #27910 ) ;
#17501=FACE_OUTER_BOUND ( 'NONE', #25921, .T. ) ;
#17521=CARTESIAN_POINT ( 'NONE',  ( -2.657516869754243061, -0.4832168877570500176, -97.49610867634444844 ) ) ;
#17665=CARTESIAN_POINT ( 'NONE',  ( 1.623446460547932624, 3.271163362686331233, -92.12187520236776095 ) ) ;
#17713=ADVANCED_FACE ( 'NONE', ( #21435 ), #30805, .T. ) ;
#17722=AXIS2_PLACEMENT_3D ( 'NONE', #2627, #14015, #29203 ) ;
#17729=DIRECTION ( 'NONE',  ( 6.901835126637476841E-14, -5.775494631892377345E-13, 1.000000000000000000 ) ) ;
#17737=DIRECTION ( 'NONE',  ( 4.250489863290715314E-14, 6.005940811918195789E-13, 1.000000000000000000 ) ) ;
#17769=( GEOMETRIC_REPRESENTATION_CONTEXT ( 3 ) GLOBAL_UNCERTAINTY_ASSIGNED_CONTEXT ( ( #6240 ) ) GLOBAL_UNIT_ASSIGNED_CONTEXT ( ( #17142, #336, #5038 ) ) REPRESENTATION_CONTEXT ( 'NONE', 'WORKASPACE' ) );
#17771=CARTESIAN_POINT ( 'NONE',  ( 0.000000000000000000, 0.000000000000000000, 231.6412452697749984 ) ) ;
#17822=CARTESIAN_POINT ( 'NONE',  ( 2.383853413490760964, -1.270093451928029582, -97.49610867634444844 ) ) ;
#17850=ADVANCED_FACE ( 'NONE', ( #22364 ), #3676, .T. ) ;
#17919=PLANE ( 'NONE',  #24300 ) ;
#17927=DIRECTION ( 'NONE',  ( -0.000000000000000000, 0.000000000000000000, -1.000000000000000000 ) ) ;
#17939=DIRECTION ( 'NONE',  ( -0.000000000000000000, 0.000000000000000000, -1.000000000000000000 ) ) ;
#17963=CIRCLE ( 'NONE', #16997, 3.500000000000000888 ) ;
#17973=CARTESIAN_POINT ( 'NONE',  ( 3.043095095518108195, -3.198806979844766474, -95.69213427724059784 ) ) ;
#18256=VERTEX_POINT ( 'NONE', #22779 ) ;
#18274=CARTESIAN_POINT ( 'NONE',  ( 3.067534055298709816, -2.342249653522415098, -93.15928300860232980 ) ) ;
#18288=EDGE_CURVE ( 'NONE', #27710, #14643, #30305, .T. ) ;
#18323=DIRECTION ( 'NONE',  ( 0.1542166437529879919, 0.9880370573969197157, 0.000000000000000000 ) ) ;
#18424=FILL_AREA_STYLE ('',( #8821 ) ) ;
#18426=CARTESIAN_POINT ( 'NONE',  ( -3.873164306258084277, -2.119290473559455101, -95.69213427732501032 ) ) ;
#18454=LINE ( 'NONE', #6649, #12255 ) ;
#18588=ORIENTED_EDGE ( 'NONE', *, *, #3819, .F. ) ;
#18662=CARTESIAN_POINT ( 'NONE',  ( 3.043095095529606997, -3.198806979771088077, -95.69213427732501032 ) ) ;
#18692=CARTESIAN_POINT ( 'NONE',  ( -2.486939662212003466, -15.93335509046200826, -109.1271631200378351 ) ) ;
#18756=AXIS2_PLACEMENT_3D ( 'NONE', #811, #24569, #7568 ) ;
#18760=ORIENTED_EDGE ( 'NONE', *, *, #22641, .F. ) ;
#18850=CONICAL_SURFACE ( 'NONE', #5294, 0.9999999999991034949, 0.7853981633970000820 ) ;
#18854=DIRECTION ( 'NONE',  ( 0.1090476345695675503, 0.6986477033489619792, 0.7071067811865496822 ) ) ;
#18874=CARTESIAN_POINT ( 'NONE',  ( 1.270718008852894654, -3.293366139498758560, 226.6412452697750268 ) ) ;
#18904=CARTESIAN_POINT ( 'NONE',  ( -3.542914729026271914, -0.003443490030646811917, -88.52261276311425320 ) ) ;
#18920=DIRECTION ( 'NONE',  ( 0.000000000000000000, 0.7113488923935485930, -0.7028390664230835805 ) ) ;
#19022=DIRECTION ( 'NONE',  ( 0.6986477033485309907, -0.1090476345690993831, -0.7071067811870476172 ) ) ;
#19028=CARTESIAN_POINT ( 'NONE',  ( -0.08634664488581689223, -3.528971028952712530, 226.6412452697750268 ) ) ;
#19074=EDGE_LOOP ( 'NONE', ( #29674, #20128, #3282, #26493 ) ) ;
#19086=ORIENTED_EDGE ( 'NONE', *, *, #26867, .T. ) ;
#19131=MECHANICAL_DESIGN_GEOMETRIC_PRESENTATION_REPRESENTATION('',(#20635),#17769);
#19162=( BOUNDED_SURFACE ( )  B_SPLINE_SURFACE ( 5, 3, ( 
 ( #7768, #24463, #29323, #1012 ),
 ( #8220, #19586, #10601, #24615 ),
 ( #22414, #12808, #25077, #26972 ),
 ( #858, #29168, #14871, #7916 ),
 ( #10301, #5409, #19897, #17521 ),
 ( #29480, #27127, #27278, #10450 ),
 ( #5562, #7614, #5718, #22103 ),
 ( #15163, #20044, #2897, #15324 ),
 ( #8070, #17665, #24767, #17211 ),
 ( #20194, #24924, #3352, #26816 ),
 ( #5261, #12959, #29788, #17822 ),
 ( #27431, #5867, #15477, #3509 ),
 ( #12492, #13106, #561, #10141 ),
 ( #19741, #1636, #3835, #11225 ),
 ( #27740, #16101, #25553, #17973 ) ),
 .UNSPECIFIED., .F., .F., .T. ) 
 B_SPLINE_SURFACE_WITH_KNOTS ( ( 6, 3, 3, 3, 6 ),
 ( 4, 4 ),
 ( 0.000000000000000000, 2.784556496770000056, 5.569112993540000112, 8.353669490309998835, 11.13822598710000022 ),
 ( 0.000000000000000000, 1.000000000000000000 ),
 .UNSPECIFIED. ) 
 GEOMETRIC_REPRESENTATION_ITEM ( )  RATIONAL_B_SPLINE_SURFACE ( (
 ( 1.000000000000000000, 0.9492530216734372805, 0.9492530216734372805, 1.000000000000000000),
 ( 1.000000000000000000, 0.9492530216734372805, 0.9492530216734372805, 1.000000000000000000),
 ( 1.000000000000000000, 0.9492530216734372805, 0.9492530216734372805, 1.000000000000000000),
 ( 1.000000000000000000, 0.9492530216734372805, 0.9492530216734372805, 1.000000000000000000),
 ( 1.000000000000000000, 0.9492530216734372805, 0.9492530216734372805, 1.000000000000000000),
 ( 1.000000000000000000, 0.9492530216734372805, 0.9492530216734372805, 1.000000000000000000),
 ( 1.000000000000000000, 0.9492530216734372805, 0.9492530216734372805, 1.000000000000000000),
 ( 1.000000000000000000, 0.9492530216734372805, 0.9492530216734372805, 1.000000000000000000),
 ( 1.000000000000000000, 0.9492530216734372805, 0.9492530216734372805, 1.000000000000000000),
 ( 1.000000000000000000, 0.9492530216734372805, 0.9492530216734372805, 1.000000000000000000),
 ( 1.000000000000000000, 0.9492530216734372805, 0.9492530216734372805, 1.000000000000000000),
 ( 1.000000000000000000, 0.9492530216734372805, 0.9492530216734372805, 1.000000000000000000),
 ( 1.000000000000000000, 0.9492530216734372805, 0.9492530216734372805, 1.000000000000000000),
 ( 1.000000000000000000, 0.9492530216734372805, 0.9492530216734372805, 1.000000000000000000),
 ( 1.000000000000000000, 0.9492530216734372805, 0.9492530216734372805, 1.000000000000000000) ) ) 
 REPRESENTATION_ITEM ( '' )  SURFACE ( )  );
#19237=ORIENTED_EDGE ( 'NONE', *, *, #23697, .F. ) ;
#19255=DIRECTION ( 'NONE',  ( 0.9880370573969196046, -0.1542166437529879364, -8.326672684677467298E-17 ) ) ;
#19274=CARTESIAN_POINT ( 'NONE',  ( -1.111846212942793288, 3.388043077328151131, -88.52261276238974119 ) ) ;
#19287=CARTESIAN_POINT ( 'NONE',  ( -3.458129700889219116, 0.5397582531354577773, 226.6412452697749984 ) ) ;
#19412=PLANE ( 'NONE',  #23597 ) ;
#19473=CIRCLE ( 'NONE', #397, 2.500000000105230491 ) ;
#19522=AXIS2_PLACEMENT_3D ( 'NONE', #24052, #5143, #2340 ) ;
#19586=CARTESIAN_POINT ( 'NONE',  ( -3.359412450346234369, 1.172221127227247806, -91.35798291625272327 ) ) ;
#19626=EDGE_LOOP ( 'NONE', ( #14561, #15492 ) ) ;
#19741=CARTESIAN_POINT ( 'NONE',  ( 3.542914729026319876, 0.003443490030938245461, -88.52261276241732446 ) ) ;
#19763=CARTESIAN_POINT ( 'NONE',  ( -3.873164306258084277, -2.119290473559455101, -95.69213427732501032 ) ) ;
#19897=CARTESIAN_POINT ( 'NONE',  ( -2.299520702359473923, 1.810397285033877646, -95.04696119083976669 ) ) ;
#19916=CARTESIAN_POINT ( 'NONE',  ( -1.823119173631714274, -0.2505752385364682366, -97.85464525912570366 ) ) ;
#20006=ORIENTED_EDGE ( 'NONE', *, *, #2792, .F. ) ;
#20044=CARTESIAN_POINT ( 'NONE',  ( 0.5703379768913079406, 3.654048244701747272, -92.17990007830465515 ) ) ;
#20128=ORIENTED_EDGE ( 'NONE', *, *, #13231, .T. ) ;
#20179=CARTESIAN_POINT ( 'NONE',  ( 2.141179080681045122, -2.824862300867048148, -90.52455892065360388 ) ) ;
#20194=CARTESIAN_POINT ( 'NONE',  ( 2.091444806099476583, 2.888061030883168456, -88.52261276238974119 ) ) ;
#20257=DIRECTION ( 'NONE',  ( -0.9880370573969196046, 0.1542166437529879086, 1.480297366166875051E-13 ) ) ;
#20304=ORIENTED_EDGE ( 'NONE', *, *, #30170, .T. ) ;
#20318=FACE_OUTER_BOUND ( 'NONE', #2819, .T. ) ;
#20332=CARTESIAN_POINT ( 'NONE',  ( 1.111846212943386591, -3.388043077324369268, -88.52261276293990022 ) ) ;
#20338=VECTOR ( 'NONE', #22212, 1000.000000000000000 ) ;
#20440=ADVANCED_BREP_SHAPE_REPRESENTATION ( '', ( #121, #17722 ), #27910 ) ;
#20455=ORIENTED_EDGE ( 'NONE', *, *, #3819, .T. ) ;
#20488=CARTESIAN_POINT ( 'NONE',  ( 1.030413743093000045, -3.909765609533090380, -92.08560516904441329 ) ) ;
#20552=CIRCLE ( 'NONE', #26093, 3.500000000000000444 ) ;
#20635=STYLED_ITEM ( 'NONE', ( #16994 ), #121 ) ;
#20646=CARTESIAN_POINT ( 'NONE',  ( 2.888061030912462801, -2.091444806055747563, -88.52261276308685467 ) ) ;
#20648=CARTESIAN_POINT ( 'NONE',  ( -3.683257989657598319, -1.493295482194435086, -96.33992724130713725 ) ) ;
#20663=ORIENTED_EDGE ( 'NONE', *, *, #16598, .F. ) ;
#20712=CARTESIAN_POINT ( 'NONE',  ( 0.5632927345713620859, -3.521042344241311017, -88.52261276296684400 ) ) ;
#20768=CARTESIAN_POINT ( 'NONE',  ( 1.692897434406342549, -3.097451722116522976, 226.6412452697750268 ) ) ;
#20792=CARTESIAN_POINT ( 'NONE',  ( -3.883058903150518049, -2.773382390028514610, -95.04434131332580193 ) ) ;
#20804=CARTESIAN_POINT ( 'NONE',  ( 3.326321175718020218, -1.384230705528964878, -93.72782450567366652 ) ) ;
#20842=EDGE_LOOP ( 'NONE', ( #135, #7507, #8934, #6974 ) ) ;
#20936=CARTESIAN_POINT ( 'NONE',  ( 0.000000000000000000, 0.000000000000000000, -85.94068374632500706 ) ) ;
#20959=PRODUCT ( 'Plunger Rod', 'Plunger Rod', '', ( #28523 ) ) ;
#20964=DIRECTION ( 'NONE',  ( 0.1090476345695682997, 0.6986477033489653099, 0.7071067811865462405 ) ) ;
#21090=CARTESIAN_POINT ( 'NONE',  ( -3.528956123591135086, 0.08598667200548251732, 226.6412452697750552 ) ) ;
#21110=CARTESIAN_POINT ( 'NONE',  ( 2.414417451572403728, -4.362164995236931908, -94.44574089077143242 ) ) ;
#21202=ADVANCED_FACE ( 'NONE', ( #22776 ), #15078, .T. ) ;
#21240=CARTESIAN_POINT ( 'NONE',  ( -3.293366139499089851, -1.270718008849189173, 226.6412452697750268 ) ) ;
#21259=FACE_OUTER_BOUND ( 'NONE', #27208, .T. ) ;
#21319=VERTEX_POINT ( 'NONE', #1695 ) ;
#21323=VECTOR ( 'NONE', #22638, 1000.000000000000000 ) ;
#21347=CARTESIAN_POINT ( 'NONE',  ( 0.000000000000000000, 0.000000000000000000, 231.1412452697749984 ) ) ;
#21416=ORIENTED_EDGE ( 'NONE', *, *, #27309, .T. ) ;
#21435=FACE_OUTER_BOUND ( 'NONE', #22379, .T. ) ;
#21483=CARTESIAN_POINT ( 'NONE',  ( 3.458129700889219116, -0.5397582531354573332, -88.52261276322501260 ) ) ;
#21537=DIRECTION ( 'NONE',  ( -0.1090476345695678556, -0.6986477033489640887, -0.7071067811865475727 ) ) ;
#21589=CARTESIAN_POINT ( 'NONE',  ( -3.507110123170089189, -0.4740316117955202246, -90.91470530330329325 ) ) ;
#21596=ORIENTED_EDGE ( 'NONE', *, *, #11873, .F. ) ;
#21607=CLOSED_SHELL ( 'NONE', ( #24275, #29237, #8654, #4969, #17850, #21202, #21628, #10140, #6685, #31032, #16698, #13640, #26975, #22403, #26096, #17713, #15055 ) ) ;
#21628=ADVANCED_FACE ( 'NONE', ( #11103 ), #6377, .T. ) ;
#21657=CARTESIAN_POINT ( 'NONE',  ( -310556.1348510272801, 168981.9135473513743, -353320.2493487302563 ) ) ;
#21754=ORIENTED_EDGE ( 'NONE', *, *, #2792, .T. ) ;
#21791=CARTESIAN_POINT ( 'NONE',  ( 1.609514238142041975, 3.181902231760902477, -88.52261276241718235 ) ) ;
#21885=FILL_AREA_STYLE_COLOUR ( '', #12839 ) ;
#21942=DIRECTION ( 'NONE',  ( 0.000000000000000000, 0.000000000000000000, 1.000000000000000000 ) ) ;
#21962=CARTESIAN_POINT ( 'NONE',  ( 1.976074114793839431, -0.3084332875059770385, 226.6412452697749984 ) ) ;
#22072=SHAPE_DEFINITION_REPRESENTATION ( #6632, #17403 ) ;
#22103=CARTESIAN_POINT ( 'NONE',  ( -1.131542931821497788, -0.1196298886178837062, -98.09067668424567898 ) ) ;
#22146=ORIENTED_EDGE ( 'NONE', *, *, #22849, .T. ) ;
#22212=DIRECTION ( 'NONE',  ( 0.000000000000000000, 0.000000000000000000, 1.000000000000000000 ) ) ;
#22233=DIRECTION ( 'NONE',  ( -0.8783853955697265015, 0.4779530278697008971, -2.498001805408841824E-13 ) ) ;
#22257=DIRECTION ( 'NONE',  ( 0.000000000000000000, 0.000000000000000000, 1.000000000000000000 ) ) ;
#22351=AXIS2_PLACEMENT_3D ( 'NONE', #6566, #25468, #13494 ) ;
#22364=FACE_OUTER_BOUND ( 'NONE', #19074, .T. ) ;
#22379=EDGE_LOOP ( 'NONE', ( #934, #17018, #4081, #18588 ) ) ;
#22403=ADVANCED_FACE ( 'NONE', ( #11455 ), #15862, .T. ) ;
#22412=ORIENTED_EDGE ( 'NONE', *, *, #25620, .F. ) ;
#22414=CARTESIAN_POINT ( 'NONE',  ( -3.181902231748757526, 1.609514238137835118, -88.52261276242234089 ) ) ;
#22531=VERTEX_POINT ( 'NONE', #29199 ) ;
#22549=DIRECTION ( 'NONE',  ( -4.250489863289427893E-14, -6.005940811918155400E-13, -1.000000000000000000 ) ) ;
#22551=CARTESIAN_POINT ( 'NONE',  ( 2.901993252043652660, -2.002183683297082517, -90.77455165165939377 ) ) ;
#22638=DIRECTION ( 'NONE',  ( 0.000000000000000000, 0.000000000000000000, 1.000000000000000000 ) ) ;
#22641=EDGE_CURVE ( 'NONE', #12690, #11998, #27895, .T. ) ;
#22649=CARTESIAN_POINT ( 'NONE',  ( 5.072625435919005586E-16, 3.702906486519338703E-16, 226.6412452697749984 ) ) ;
#22678=EDGE_LOOP ( 'NONE', ( #5924, #28058, #7892, #20663, #12684 ) ) ;
#22703=VERTEX_POINT ( 'NONE', #17207 ) ;
#22776=FACE_OUTER_BOUND ( 'NONE', #15597, .T. ) ;
#22779=CARTESIAN_POINT ( 'NONE',  ( -1.976074114793839431, 0.3084332875059763723, 231.1412452697749984 ) ) ;
#22796=ORIENTED_EDGE ( 'NONE', *, *, #11925, .T. ) ;
#22816=CIRCLE ( 'NONE', #26835, 2.500000000105230491 ) ;
#22844=CARTESIAN_POINT ( 'NONE',  ( -2.490109544994508539, -4.523857212610923995, -93.52962329550673815 ) ) ;
#22849=EDGE_CURVE ( 'NONE', #13901, #6489, #12821, .T. ) ;
#22856=CARTESIAN_POINT ( 'NONE',  ( 0.3014737666566600360, -5.198467272794965233, -93.29359154310911606 ) ) ;
#23016=CARTESIAN_POINT ( 'NONE',  ( 3.458129700891746428, -0.5397582531192768318, -88.52261276316077954 ) ) ;
#23067=EDGE_LOOP ( 'NONE', ( #9754, #14017 ) ) ;
#23097=CARTESIAN_POINT ( 'NONE',  ( -1.976074114793839431, 0.3084332875059763723, 226.6412452697749984 ) ) ;
#23143=CARTESIAN_POINT ( 'NONE',  ( -2.213834474261364260, -2.749352377424092442, 226.6412452697750268 ) ) ;
#23163=CARTESIAN_POINT ( 'NONE',  ( -1.249369445655645006, -5.033661498259376366, -93.21726054315608678 ) ) ;
#23172=CARTESIAN_POINT ( 'NONE',  ( -2.914123423697624116, -2.127246859470591112, -88.52261276302716908 ) ) ;
#23272=EDGE_LOOP ( 'NONE', ( #20455, #25181, #20304 ) ) ;
#23335=CARTESIAN_POINT ( 'NONE',  ( -2.595987296770100095, -16.63200279373747392, -109.8342699011499946 ) ) ;
#23402=FACE_OUTER_BOUND ( 'NONE', #19626, .T. ) ;
#23411=STYLED_ITEM ( 'NONE', ( #24085 ), #20440 ) ;
#23488=CARTESIAN_POINT ( 'NONE',  ( -3.494139924891833893, -1.791588778288840000, -92.88964426498927196 ) ) ;
#23558=CARTESIAN_POINT ( 'NONE',  ( -3.458129700889219116, 0.5397582531354577773, -88.52261276322501260 ) ) ;
#23564=PRODUCT_DEFINITION_CONTEXT ( 'detailed design', #1543, 'design' ) ;
#23597=AXIS2_PLACEMENT_3D ( 'NONE', #4791, #5240, #19255 ) ;
#23630=ORIENTED_EDGE ( 'NONE', *, *, #5060, .F. ) ;
#23642=CARTESIAN_POINT ( 'NONE',  ( -3.213922572545196310, -4.048003670336641768, -93.88815951138718674 ) ) ;
#23697=EDGE_CURVE ( 'NONE', #12690, #13120, #3738, .T. ) ;
#23706=CARTESIAN_POINT ( 'NONE',  ( 3.458129700889219116, -0.5397582531354573332, -88.52261276322501260 ) ) ;
#23708=LINE ( 'NONE', #14415, #11555 ) ;
#23833=CARTESIAN_POINT ( 'NONE',  ( 0.000000000000000000, 0.000000000000000000, 226.6412452707750163 ) ) ;
#23842=CIRCLE ( 'NONE', #14289, 3.500000000000000888 ) ;
#23848=CIRCLE ( 'NONE', #6237, 2.000000000000000000 ) ;
#23862=CONICAL_SURFACE ( 'NONE', #9765, 2.500000000105231823, 0.7853981633974348453 ) ;
#23936=SURFACE_SIDE_STYLE ('',( #7241 ) ) ;
#24006=CARTESIAN_POINT ( 'NONE',  ( 3.388043077353672494, 1.111846212962369629, -88.52261276243450538 ) ) ;
#24020=EDGE_CURVE ( 'NONE', #8030, #13901, #23842, .T. ) ;
#24052=CARTESIAN_POINT ( 'NONE',  ( -2.595987296770100095, -16.63200279373747392, -109.8342699011499946 ) ) ;
#24085=PRESENTATION_STYLE_ASSIGNMENT (( #16370 ) ) ;
#24122=EDGE_LOOP ( 'NONE', ( #9151, #9181, #5688, #7738 ) ) ;
#24218=EDGE_CURVE ( 'NONE', #22703, #18256, #25839, .T. ) ;
#24275=ADVANCED_FACE ( 'NONE', ( #700 ), #23862, .T. ) ;
#24300=AXIS2_PLACEMENT_3D ( 'NONE', #17771, #15724, #25340 ) ;
#24356=DIRECTION ( 'NONE',  ( 0.6215393814730896249, -0.6030661632640409442, -0.5000000000040381032 ) ) ;
#24379=EDGE_CURVE ( 'NONE', #21319, #27710, #8235, .T. ) ;
#24386=ORIENTED_EDGE ( 'NONE', *, *, #30170, .F. ) ;
#24463=CARTESIAN_POINT ( 'NONE',  ( -3.444197478484224195, 0.6290193840551402404, -91.21022378307108625 ) ) ;
#24569=DIRECTION ( 'NONE',  ( -6.901835126637476841E-14, 5.775494631892377345E-13, -1.000000000000000000 ) ) ;
#24598=DIRECTION ( 'NONE',  ( 0.8783853955697265015, -0.4779530278697008971, 2.498001805408841824E-13 ) ) ;
#24600=LINE ( 'NONE', #12788, #10667 ) ;
#24615=CARTESIAN_POINT ( 'NONE',  ( -3.813212237922182002, -1.735188837432927178, -96.08088653434137427 ) ) ;
#24667=ORIENTED_EDGE ( 'NONE', *, *, #23697, .T. ) ;
#24690=ORIENTED_EDGE ( 'NONE', *, *, #3871, .T. ) ;
#24752=CARTESIAN_POINT ( 'NONE',  ( 3.458129700889219116, -0.5397582531354573332, -88.52261276322501260 ) ) ;
#24767=CARTESIAN_POINT ( 'NONE',  ( 1.423903527214286813, 1.992729285291204633, -95.48173244568418738 ) ) ;
#24903=( GEOMETRIC_REPRESENTATION_CONTEXT ( 3 ) GLOBAL_UNCERTAINTY_ASSIGNED_CONTEXT ( ( #3366 ) ) GLOBAL_UNIT_ASSIGNED_CONTEXT ( ( #11960, #26441, #9284 ) ) REPRESENTATION_CONTEXT ( 'NONE', 'WORKASPACE' ) );
#24923=VERTEX_POINT ( 'NONE', #25815 ) ;
#24924=CARTESIAN_POINT ( 'NONE',  ( 2.105377028506504988, 2.977322161815887380, -92.06382165379619664 ) ) ;
#25055=CARTESIAN_POINT ( 'NONE',  ( 4.239428892460699881E-14, 6.006117008548172241E-13, 232.1412452697749984 ) ) ;
#25077=CARTESIAN_POINT ( 'NONE',  ( -3.331151133293480893, 0.6533045715718522883, -94.29636648343951322 ) ) ;
#25136=DIRECTION ( 'NONE',  ( 0.9880370573969197157, -0.1542166437529880474, 0.000000000000000000 ) ) ;
#25181=ORIENTED_EDGE ( 'NONE', *, *, #11873, .T. ) ;
#25200=CARTESIAN_POINT ( 'NONE',  ( 3.043095095529606997, -3.198806979771088077, -95.69213427732501032 ) ) ;
#25256=CARTESIAN_POINT ( 'NONE',  ( 1.915963263359339530, -10.42012882710465682, -88.85875473022500159 ) ) ;
#25340=DIRECTION ( 'NONE',  ( -0.9880370573969196046, 0.1542166437529879364, 0.000000000000000000 ) ) ;
#25378=CARTESIAN_POINT ( 'NONE',  ( -1.687520611373146684, -3.681674406733895122, -91.97391714452653844 ) ) ;
#25444=CARTESIAN_POINT ( 'NONE',  ( 3.373344672752164985, -1.082959996301563477, -88.52261276311425320 ) ) ;
#25466=CARTESIAN_POINT ( 'NONE',  ( 0.000000000000000000, 0.000000000000000000, 231.1412452697749984 ) ) ;
#25468=DIRECTION ( 'NONE',  ( -0.1090476345695678556, -0.6986477033489640887, -0.7071067811865475727 ) ) ;
#25533=CARTESIAN_POINT ( 'NONE',  ( 3.250256321940253823, -1.871563930198836712, -93.44355375713804790 ) ) ;
#25553=CARTESIAN_POINT ( 'NONE',  ( 3.326321151026052636, -1.384230863725755878, -93.72782493932767522 ) ) ;
#25620=EDGE_CURVE ( 'NONE', #7336, #13982, #26468, .T. ) ;
#25754=CARTESIAN_POINT ( 'NONE',  ( 1.111846212943386591, -3.388043077324369268, -88.52261276293990022 ) ) ;
#25815=CARTESIAN_POINT ( 'NONE',  ( -0.1258946531760308241, -17.01754440315029271, -109.8342699011357126 ) ) ;
#25839=CIRCLE ( 'NONE', #16787, 2.000000000000000000 ) ;
#25873=AXIS2_PLACEMENT_3D ( 'NONE', #25256, #10934, #18323 ) ;
#25921=EDGE_LOOP ( 'NONE', ( #28742, #5457, #8536, #29949 ) ) ;
#25946=DIRECTION ( 'NONE',  ( 0.000000000000000000, 0.7113488923935522568, -0.7028390664230799167 ) ) ;
#26002=DIRECTION ( 'NONE',  ( 0.000000000000000000, -0.7113488923935499253, 0.7028390664230821372 ) ) ;
#26021=CIRCLE ( 'NONE', #5892, 2.000000000000000000 ) ;
#26093=AXIS2_PLACEMENT_3D ( 'NONE', #23833, #2278, #11863 ) ;
#26096=ADVANCED_FACE ( 'NONE', ( #2513 ), #26729, .T. ) ;
#26264=CARTESIAN_POINT ( 'NONE',  ( 349323.8516742420034, -54523.81728454602126, -353320.2493477302487 ) ) ;
#26297=ORIENTED_EDGE ( 'NONE', *, *, #1841, .F. ) ;
#26350=DIRECTION ( 'NONE',  ( -0.9880370573969197157, 0.1542166437529879364, 0.000000000000000000 ) ) ;
#26359=VECTOR ( 'NONE', #14766, 1000.000000000000114 ) ;
#26408=VECTOR ( 'NONE', #16387, 1000.000000000000114 ) ;
#26440=ORIENTED_EDGE ( 'NONE', *, *, #24218, .T. ) ;
#26441=( NAMED_UNIT ( * ) PLANE_ANGLE_UNIT ( ) SI_UNIT ( $, .RADIAN. ) );
#26468=LINE ( 'NONE', #12301, #20338 ) ;
#26493=ORIENTED_EDGE ( 'NONE', *, *, #18288, .F. ) ;
#26525=DIRECTION ( 'NONE',  ( -0.6211122697021861372, 0.3379638270947744605, -0.7071067811871500908 ) ) ;
#26587=ORIENTED_EDGE ( 'NONE', *, *, #4438, .T. ) ;
#26654=CARTESIAN_POINT ( 'NONE',  ( 0.000000000000000000, 0.000000000000000000, 231.1412452697749984 ) ) ;
#26662=VERTEX_POINT ( 'NONE', #3083 ) ;
#26682=CARTESIAN_POINT ( 'NONE',  ( 3.043095095529606997, -3.198806979771088077, -95.69213427732501032 ) ) ;
#26729=CYLINDRICAL_SURFACE ( 'NONE', #14270, 3.500000000000000444 ) ;
#26816=CARTESIAN_POINT ( 'NONE',  ( 1.532951308181600414, -0.6901018627532701233, -97.93793859254537892 ) ) ;
#26835=AXIS2_PLACEMENT_3D ( 'NONE', #30885, #9315, #16552 ) ;
#26837=CARTESIAN_POINT ( 'NONE',  ( 2.015353881180397710, -1.035356480594303852, -97.67120874164949385 ) ) ;
#26848=APPLICATION_CONTEXT ( 'automotive_design' ) ;
#26857=AXIS2_PLACEMENT_3D ( 'NONE', #10902, #29630, #849 ) ;
#26867=EDGE_CURVE ( 'NONE', #11998, #6070, #2014, .T. ) ;
#26883=CARTESIAN_POINT ( 'NONE',  ( 0.000000000000000000, 0.000000000000000000, 229.1412452697749984 ) ) ;
#26964=CARTESIAN_POINT ( 'NONE',  ( -2.595987296770100095, -16.63200279373747392, -109.8342699011499946 ) ) ;
#26972=CARTESIAN_POINT ( 'NONE',  ( -3.646602756718712701, -1.367734702628457866, -96.46963879144223597 ) ) ;
#26975=ADVANCED_FACE ( 'NONE', ( #29642 ), #19162, .T. ) ;
#27098=CARTESIAN_POINT ( 'NONE',  ( 0.000000000000000000, 0.000000000000000000, -85.94068374632500706 ) ) ;
#27127=CARTESIAN_POINT ( 'NONE',  ( -1.097913990535764883, 3.477304208260869167, -92.06382165379621085 ) ) ;
#27208=EDGE_LOOP ( 'NONE', ( #13505, #21596, #15570, #6728 ) ) ;
#27275=EDGE_CURVE ( 'NONE', #14643, #21319, #215, .T. ) ;
#27278=CARTESIAN_POINT ( 'NONE',  ( -1.294030826674742229, 2.220820491787859119, -95.37004441182592984 ) ) ;
#27309=EDGE_CURVE ( 'NONE', #6070, #26662, #3754, .T. ) ;
#27343=EDGE_CURVE ( 'NONE', #22531, #8030, #17116, .T. ) ;
#27413=CARTESIAN_POINT ( 'NONE',  ( -2.363020471776699605, -4.627995288602582136, -93.44632962453067648 ) ) ;
#27431=CARTESIAN_POINT ( 'NONE',  ( 3.388043077353672494, 1.111846212962369629, -88.52261276243450538 ) ) ;
#27477=VERTEX_POINT ( 'NONE', #23097 ) ;
#27562=CARTESIAN_POINT ( 'NONE',  ( 3.181902231748806376, -1.609514238137543796, -88.52261276306772686 ) ) ;
#27612=DIRECTION ( 'NONE',  ( 0.000000000000000000, 0.000000000000000000, 1.000000000000000000 ) ) ;
#27629=CARTESIAN_POINT ( 'NONE',  ( -3.458129700889219116, 0.5397582531354577773, -88.52261276322501260 ) ) ;
#27710=VERTEX_POINT ( 'NONE', #11442 ) ;
#27740=CARTESIAN_POINT ( 'NONE',  ( 3.458129700887829561, -0.5397582531443678722, -88.52261276240527366 ) ) ;
#27895=CIRCLE ( 'NONE', #16839, 10.00564797610000056 ) ;
#27910=( GEOMETRIC_REPRESENTATION_CONTEXT ( 3 ) GLOBAL_UNCERTAINTY_ASSIGNED_CONTEXT ( ( #17225 ) ) GLOBAL_UNIT_ASSIGNED_CONTEXT ( ( #15586, #1753, #15744 ) ) REPRESENTATION_CONTEXT ( 'NONE', 'WORKASPACE' ) );
#27942=EDGE_CURVE ( 'NONE', #13120, #6070, #13793, .T. ) ;
#28004=CARTESIAN_POINT ( 'NONE',  ( -0.9931698613850974411, -3.387288372825724814, 226.6412452697749984 ) ) ;
#28034=CARTESIAN_POINT ( 'NONE',  ( -3.528982507896216703, 0.08581763272074406645, -91.06246442329681656 ) ) ;
#28058=ORIENTED_EDGE ( 'NONE', *, *, #11751, .T. ) ;
#28068=EDGE_LOOP ( 'NONE', ( #2194, #3953, #2331 ) ) ;
#28070=VECTOR ( 'NONE', #24356, 1000.000000000000114 ) ;
#28253=CARTESIAN_POINT ( 'NONE',  ( 2.127246859547380353, -2.914123423641564070, -88.52261276302716908 ) ) ;
#28277=DIRECTION ( 'NONE',  ( -0.9880370573969197157, 0.1542166437529879364, 0.000000000000000000 ) ) ;
#28457=CARTESIAN_POINT ( 'NONE',  ( -2.486939662212004354, -18.42307621383944749, -106.6672263875570650 ) ) ;
#28471=CARTESIAN_POINT ( 'NONE',  ( 2.434303047052905011, -2.556415643317960562, 226.6412452697750552 ) ) ;
#28518=CARTESIAN_POINT ( 'NONE',  ( -2.486939662212006130, -15.93335509046202247, -109.1271631200378494 ) ) ;
#28523=PRODUCT_CONTEXT ( 'NONE', #26848, 'mechanical' ) ;
#28615=CARTESIAN_POINT ( 'NONE',  ( -2.595987296770099206, -16.63200279373747037, -109.8342699011499946 ) ) ;
#28703=CARTESIAN_POINT ( 'NONE',  ( -5.072625435919005586E-16, -3.702906486519338703E-16, 226.6412452697749984 ) ) ;
#28742=ORIENTED_EDGE ( 'NONE', *, *, #4438, .F. ) ;
#29091=DIRECTION ( 'NONE',  ( -0.9880370573969196046, 0.1542166437529880751, 0.000000000000000000 ) ) ;
#29168=CARTESIAN_POINT ( 'NONE',  ( -2.874128808496339893, 2.180705937046730547, -91.64589571366730070 ) ) ;
#29169=ORIENTED_EDGE ( 'NONE', *, *, #24218, .F. ) ;
#29199=CARTESIAN_POINT ( 'NONE',  ( -2.595987296770099650, -18.41037502479620969, -108.0771722350183381 ) ) ;
#29203=DIRECTION ( 'NONE',  ( 1.000000000000000000, 0.000000000000000000, 0.000000000000000000 ) ) ;
#29237=ADVANCED_FACE ( 'NONE', ( #13057 ), #17919, .T. ) ;
#29323=CARTESIAN_POINT ( 'NONE',  ( -3.589938250752385596, -0.3047143574548395462, -93.72782493932767522 ) ) ;
#29347=CARTESIAN_POINT ( 'NONE',  ( -3.244486662300113622, -0.9559324580886872091, -96.93852766387357178 ) ) ;
#29436=EDGE_CURVE ( 'NONE', #790, #26662, #11689, .T. ) ;
#29480=CARTESIAN_POINT ( 'NONE',  ( -1.111846212942793288, 3.388043077328151131, -88.52261276238974119 ) ) ;
#29503=CARTESIAN_POINT ( 'NONE',  ( 2.584869084651857385, -1.587944713799994467, -97.21305981300143628 ) ) ;
#29630=DIRECTION ( 'NONE',  ( 4.250489863290715314E-14, 6.005940811918195789E-13, 1.000000000000000000 ) ) ;
#29642=FACE_OUTER_BOUND ( 'NONE', #10402, .T. ) ;
#29674=ORIENTED_EDGE ( 'NONE', *, *, #7138, .T. ) ;
#29701=DIRECTION ( 'NONE',  ( 0.000000000000000000, 0.000000000000000000, 1.000000000000000000 ) ) ;
#29770=CARTESIAN_POINT ( 'NONE',  ( -2.172877275949271159, -3.409783563088108149, -92.08560516904439908 ) ) ;
#29788=CARTESIAN_POINT ( 'NONE',  ( 2.741849580885529658, 1.023520720862898248, -95.04696119083976669 ) ) ;
#29821=EDGE_CURVE ( 'NONE', #13982, #22703, #23848, .T. ) ;
#29918=CYLINDRICAL_SURFACE ( 'NONE', #16064, 3.500000000000000444 ) ;
#29930=CARTESIAN_POINT ( 'NONE',  ( 0.4852863613287607958, -4.020814519287960742, -91.97391714452653844 ) ) ;
#29944=ORIENTED_EDGE ( 'NONE', *, *, #16598, .T. ) ;
#29949=ORIENTED_EDGE ( 'NONE', *, *, #29821, .T. ) ;
#30020=DIRECTION ( 'NONE',  ( -0.9880370573969196046, 0.1542166437529879086, -5.551115123125782071E-14 ) ) ;
#30027=AXIS2_PLACEMENT_3D ( 'NONE', #3029, #12622, #22233 ) ;
#30088=CARTESIAN_POINT ( 'NONE',  ( -0.6309877232518290580, -4.042619772830049918, -91.86228428259488510 ) ) ;
#30133=CARTESIAN_POINT ( 'NONE',  ( -2.486939662212003466, -15.93335509046200826, -109.1271631200378351 ) ) ;
#30170=EDGE_CURVE ( 'NONE', #22531, #1522, #22816, .T. ) ;
#30243=CARTESIAN_POINT ( 'NONE',  ( 2.816533608213001916, -3.950362352052525061, -94.91462932778338768 ) ) ;
#30246=CARTESIAN_POINT ( 'NONE',  ( -2.945834232371903116, -0.7246911579439561102, -97.21305981300695009 ) ) ;
#30296=DIRECTION ( 'NONE',  ( -0.9880370573969197157, 0.1542166437529879364, 0.000000000000000000 ) ) ;
#30305=CIRCLE ( 'NONE', #16724, 1.500000000000000222 ) ;
#30411=CARTESIAN_POINT ( 'NONE',  ( 3.472061922019873403, -0.4504971303802423610, -91.21022354329026882 ) ) ;
#30554=CARTESIAN_POINT ( 'NONE',  ( 2.115765021644385069, -4.593406295380427551, -94.17120874163683197 ) ) ;
#30591=EDGE_CURVE ( 'NONE', #27477, #18256, #18454, .T. ) ;
#30706=CARTESIAN_POINT ( 'NONE',  ( -1.691925696239311883, -4.899391353707211572, -93.28167488203875735 ) ) ;
#30805=CONICAL_SURFACE ( 'NONE', #17221, 2.500000000105226938, 0.7853981633974418397 ) ;
#30831=CARTESIAN_POINT ( 'NONE',  ( 0.9711900386741275648, -16.47311334361725343, -109.1271631200178689 ) ) ;
#30837=CARTESIAN_POINT ( 'NONE',  ( -2.556415643314931874, -2.434303047057058134, 226.6412452697750837 ) ) ;
#30874=CARTESIAN_POINT ( 'NONE',  ( -3.005466662781860698, -2.712465827810011110, -92.40868836340081316 ) ) ;
#30885=CARTESIAN_POINT ( 'NONE',  ( -2.595987296770100095, -16.63200279373747392, -109.8342699011499946 ) ) ;
#30891=EDGE_LOOP ( 'NONE', ( #21754, #18760, #16412, #5219 ) ) ;
#30944=DIRECTION ( 'NONE',  ( 0.000000000000000000, 0.000000000000000000, 1.000000000000000000 ) ) ;
#31022=( BOUNDED_SURFACE ( )  B_SPLINE_SURFACE ( 5, 3, ( 
 ( #23016, #30411, #20804, #11054 ),
 ( #3334, #15923, #25533, #3643 ),
 ( #27562, #6162, #18274, #30243 ),
 ( #20646, #22551, #5699, #8357 ),
 ( #1139, #20179, #10732, #6008 ),
 ( #20332, #8202, #20488, #15306 ),
 ( #15606, #13239, #29930, #22856 ),
 ( #1302, #10896, #30088, #8514 ),
 ( #15764, #10585, #25378, #12943 ),
 ( #8674, #13566, #29770, #27413 ),
 ( #23172, #16080, #30874, #23642 ),
 ( #11517, #11831, #23488, #4285 ),
 ( #1926, #21589, #9304, #11671 ),
 ( #18904, #28034, #8993, #8831 ),
 ( #6947, #6478, #11977, #2079 ) ),
 .UNSPECIFIED., .F., .F., .T. ) 
 B_SPLINE_SURFACE_WITH_KNOTS ( ( 6, 3, 3, 3, 6 ),
 ( 4, 4 ),
 ( 10.99557428763625744, 13.78013078440000072, 16.56468728109999944, 19.34924377789999994, 22.13380027456373966 ),
 ( 0.000000000000000000, 1.000000000000000000 ),
 .UNSPECIFIED. ) 
 GEOMETRIC_REPRESENTATION_ITEM ( )  RATIONAL_B_SPLINE_SURFACE ( (
 ( 1.000000000000000000, 0.9492530301840010898, 0.9492530301840010898, 1.000000000000000000),
 ( 1.000000000000000000, 0.9492530301840010898, 0.9492530301840010898, 1.000000000000000000),
 ( 1.000000000000000000, 0.9492530301840010898, 0.9492530301840010898, 1.000000000000000000),
 ( 1.000000000000000000, 0.9492530301840010898, 0.9492530301840010898, 1.000000000000000000),
 ( 1.000000000000000000, 0.9492530301840010898, 0.9492530301840010898, 1.000000000000000000),
 ( 1.000000000000000000, 0.9492530301840010898, 0.9492530301840010898, 1.000000000000000000),
 ( 1.000000000000000000, 0.9492530301840010898, 0.9492530301840010898, 1.000000000000000000),
 ( 1.000000000000000000, 0.9492530301840010898, 0.9492530301840010898, 1.000000000000000000),
 ( 1.000000000000000000, 0.9492530301840010898, 0.9492530301840010898, 1.000000000000000000),
 ( 1.000000000000000000, 0.9492530301840010898, 0.9492530301840010898, 1.000000000000000000),
 ( 1.000000000000000000, 0.9492530301840010898, 0.9492530301840010898, 1.000000000000000000),
 ( 1.000000000000000000, 0.9492530301840010898, 0.9492530301840010898, 1.000000000000000000),
 ( 1.000000000000000000, 0.9492530301840010898, 0.9492530301840010898, 1.000000000000000000),
 ( 1.000000000000000000, 0.9492530301840010898, 0.9492530301840010898, 1.000000000000000000),
 ( 1.000000000000000000, 0.9492530301840010898, 0.9492530301840010898, 1.000000000000000000) ) ) 
 REPRESENTATION_ITEM ( '' )  SURFACE ( )  );
#31032=ADVANCED_FACE ( 'NONE', ( #1591 ), #3790, .T. ) ;
#31091=VECTOR ( 'NONE', #22257, 1000.000000000000000 ) ;
ENDSEC;
END-ISO-10303-21;
